ISO-10303-21;
HEADER;
/* Generated by software containing ST-Developer
 * from STEP Tools, Inc. (www.steptools.com) 
 */

FILE_DESCRIPTION(
/* description */ ('Timing belt drive module 2 mm Pitch Timing 20T-40T'),

/* implementation_level */ '2;1');

FILE_NAME(
/* name */ 'M4 clamp nut (2).step',
/* time_stamp */ '2026-10-28T03:25:12-07:00',
/* author */ (''),
/* organization */ (''),
/* preprocessor_version */ 'ST-DEVELOPER v20.2',
/* originating_system */ 'Autodesk Translation Framework v15.17.0.0',
/* authorisation */ '');

FILE_SCHEMA (('AUTOMOTIVE_DESIGN { 1 0 10303 214 3 1 1 }'));
ENDSEC;

DATA;
#10=MECHANICAL_DESIGN_GEOMETRIC_PRESENTATION_REPRESENTATION('',(#534),#17830);
#448=SHAPE_REPRESENTATION_RELATIONSHIP('SRR','None',#18018,#491);
#491=ADVANCED_BREP_SHAPE_REPRESENTATION('',(#592),#17793);
#534=STYLED_ITEM('',(#18324),#592);
#592=MANIFOLD_SOLID_BREP('Body1',#8991);
#695=FACE_BOUND('',#1662,.T.);
#696=FACE_BOUND('',#1664,.T.);
#835=PLANE('',#9769);
#836=PLANE('',#9770);
#1080=FACE_OUTER_BOUND('',#1659,.T.);
#1081=FACE_OUTER_BOUND('',#1660,.T.);
#1082=FACE_OUTER_BOUND('',#1661,.T.);
#1083=FACE_OUTER_BOUND('',#1663,.T.);
#1659=EDGE_LOOP('',(#6337,#6338,#6339,#6340));
#1660=EDGE_LOOP('',(#6341,#6342,#6343,#6344));
#1661=EDGE_LOOP('',(#6345));
#1662=EDGE_LOOP('',(#6346));
#1663=EDGE_LOOP('',(#6347));
#1664=EDGE_LOOP('',(#6348));
#2256=CIRCLE('',#9764,0.164999999999999);
#2257=CIRCLE('',#9765,0.164999999999999);
#2258=CIRCLE('',#9767,0.4);
#2259=CIRCLE('',#9768,0.4);
#2956=LINE('',#14478,#3434);
#2957=LINE('',#14484,#3435);
#3434=VECTOR('',#11473,0.164999999999999);
#3435=VECTOR('',#11480,0.4);
#3934=VERTEX_POINT('',#14475);
#3935=VERTEX_POINT('',#14477);
#3936=VERTEX_POINT('',#14481);
#3937=VERTEX_POINT('',#14483);
#4851=EDGE_CURVE('',#3934,#3934,#2256,.T.);
#4852=EDGE_CURVE('',#3934,#3935,#2956,.T.);
#4853=EDGE_CURVE('',#3935,#3935,#2257,.T.);
#4854=EDGE_CURVE('',#3936,#3936,#2258,.T.);
#4855=EDGE_CURVE('',#3936,#3937,#2957,.T.);
#4856=EDGE_CURVE('',#3937,#3937,#2259,.T.);
#6337=ORIENTED_EDGE('',*,*,#4851,.F.);
#6338=ORIENTED_EDGE('',*,*,#4852,.T.);
#6339=ORIENTED_EDGE('',*,*,#4853,.T.);
#6340=ORIENTED_EDGE('',*,*,#4852,.F.);
#6341=ORIENTED_EDGE('',*,*,#4854,.F.);
#6342=ORIENTED_EDGE('',*,*,#4855,.T.);
#6343=ORIENTED_EDGE('',*,*,#4856,.T.);
#6344=ORIENTED_EDGE('',*,*,#4855,.F.);
#6345=ORIENTED_EDGE('',*,*,#4854,.T.);
#6346=ORIENTED_EDGE('',*,*,#4851,.T.);
#6347=ORIENTED_EDGE('',*,*,#4856,.F.);
#6348=ORIENTED_EDGE('',*,*,#4853,.F.);
#8237=CYLINDRICAL_SURFACE('',#9763,0.164999999999999);
#8238=CYLINDRICAL_SURFACE('',#9766,0.4);
#8578=ADVANCED_FACE('',(#1080),#8237,.F.);
#8579=ADVANCED_FACE('',(#1081),#8238,.T.);
#8580=ADVANCED_FACE('',(#1082,#695),#835,.T.);
#8581=ADVANCED_FACE('',(#1083,#696),#836,.F.);
#8991=CLOSED_SHELL('',(#8578,#8579,#8580,#8581));
#9762=AXIS2_PLACEMENT_3D('',#14473,#11467,#11468);
#9763=AXIS2_PLACEMENT_3D('',#14474,#11469,#11470);
#9764=AXIS2_PLACEMENT_3D('',#14476,#11471,#11472);
#9765=AXIS2_PLACEMENT_3D('',#14479,#11474,#11475);
#9766=AXIS2_PLACEMENT_3D('',#14480,#11476,#11477);
#9767=AXIS2_PLACEMENT_3D('',#14482,#11478,#11479);
#9768=AXIS2_PLACEMENT_3D('',#14485,#11481,#11482);
#9769=AXIS2_PLACEMENT_3D('',#14486,#11483,#11484);
#9770=AXIS2_PLACEMENT_3D('',#14487,#11485,#11486);
#11467=DIRECTION('axis',(0.,0.,1.));
#11468=DIRECTION('refdir',(1.,0.,0.));
#11469=DIRECTION('center_axis',(0.,0.,1.));
#11470=DIRECTION('ref_axis',(1.,0.,0.));
#11471=DIRECTION('center_axis',(0.,0.,-1.));
#11472=DIRECTION('ref_axis',(1.,0.,0.));
#11473=DIRECTION('',(0.,0.,-1.));
#11474=DIRECTION('center_axis',(0.,0.,-1.));
#11475=DIRECTION('ref_axis',(1.,0.,0.));
#11476=DIRECTION('center_axis',(0.,0.,1.));
#11477=DIRECTION('ref_axis',(1.,0.,0.));
#11478=DIRECTION('center_axis',(0.,0.,1.));
#11479=DIRECTION('ref_axis',(1.,0.,0.));
#11480=DIRECTION('',(0.,0.,-1.));
#11481=DIRECTION('center_axis',(0.,0.,1.));
#11482=DIRECTION('ref_axis',(1.,0.,0.));
#11483=DIRECTION('center_axis',(0.,0.,1.));
#11484=DIRECTION('ref_axis',(1.,0.,0.));
#11485=DIRECTION('center_axis',(0.,0.,1.));
#11486=DIRECTION('ref_axis',(1.,0.,0.));
#14473=CARTESIAN_POINT('',(0.,0.,0.));
#14474=CARTESIAN_POINT('Origin',(9.77091003018116,-1.,-1.6));
#14475=CARTESIAN_POINT('',(9.60591003018116,-1.,-1.2));
#14476=CARTESIAN_POINT('Origin',(9.77091003018116,-1.,-1.2));
#14477=CARTESIAN_POINT('',(9.60591003018116,-1.,-1.6));
#14478=CARTESIAN_POINT('',(9.60591003018116,-1.,-1.6));
#14479=CARTESIAN_POINT('Origin',(9.77091003018116,-1.,-1.6));
#14480=CARTESIAN_POINT('Origin',(9.77091003018116,-1.,-1.6));
#14481=CARTESIAN_POINT('',(9.37091003018116,-1.,-1.2));
#14482=CARTESIAN_POINT('Origin',(9.77091003018116,-1.,-1.2));
#14483=CARTESIAN_POINT('',(9.37091003018116,-1.,-1.6));
#14484=CARTESIAN_POINT('',(9.37091003018116,-1.,-1.6));
#14485=CARTESIAN_POINT('Origin',(9.77091003018116,-1.,-1.6));
#14486=CARTESIAN_POINT('Origin',(9.77091003018116,-1.,-1.2));
#14487=CARTESIAN_POINT('Origin',(9.77091003018116,-1.,-1.6));
#17743=UNCERTAINTY_MEASURE_WITH_UNIT(LENGTH_MEASURE(0.001),#17831,
'DISTANCE_ACCURACY_VALUE',
'Maximum model space distance between geometric entities at asserted c
onnectivities');
#17780=UNCERTAINTY_MEASURE_WITH_UNIT(LENGTH_MEASURE(0.001),#17831,
'DISTANCE_ACCURACY_VALUE',
'Maximum model space distance between geometric entities at asserted c
onnectivities');
#17793=(
GEOMETRIC_REPRESENTATION_CONTEXT(3)
GLOBAL_UNCERTAINTY_ASSIGNED_CONTEXT((#17743))
GLOBAL_UNIT_ASSIGNED_CONTEXT((#17831,#17833,#17834))
REPRESENTATION_CONTEXT('','3D')
);
#17830=(
GEOMETRIC_REPRESENTATION_CONTEXT(3)
GLOBAL_UNCERTAINTY_ASSIGNED_CONTEXT((#17780))
GLOBAL_UNIT_ASSIGNED_CONTEXT((#17831,#17833,#17834))
REPRESENTATION_CONTEXT('','3D')
);
#17831=(
LENGTH_UNIT()
NAMED_UNIT(*)
SI_UNIT(.CENTI.,.METRE.)
);
#17833=(
NAMED_UNIT(*)
PLANE_ANGLE_UNIT()
SI_UNIT($,.RADIAN.)
);
#17834=(
NAMED_UNIT(*)
SI_UNIT($,.STERADIAN.)
SOLID_ANGLE_UNIT()
);
#17847=SHAPE_DEFINITION_REPRESENTATION(#17896,#18018);
#17896=PRODUCT_DEFINITION_SHAPE('',$,#18068);
#18018=SHAPE_REPRESENTATION('',(#9762),#17793);
#18055=PRODUCT_DEFINITION_CONTEXT('part definition',#18204,'design');
#18068=PRODUCT_DEFINITION('M4 clamp nut (2)','M4 clamp nut (2)',#18117,#18055);
#18117=PRODUCT_DEFINITION_FORMATION('',$,#18218);
#18204=APPLICATION_CONTEXT(
'Core Data for Automotive Mechanical Design Process');
#18205=PRODUCT_CONTEXT('part definition',#18204,'mechanical');
#18218=PRODUCT('M4 clamp nut (2)','M4 clamp nut (2)','M4 clamp nut (2)',(#18205));
#18318=COLOUR_RGB('Black',0.12,0.14,0.17);
#18319=FILL_AREA_STYLE_COLOUR('',#18318);
#18320=FILL_AREA_STYLE('',(#18319));
#18321=SURFACE_STYLE_FILL_AREA(#18320);
#18322=SURFACE_SIDE_STYLE('',(#18321));
#18323=SURFACE_STYLE_USAGE(.BOTH.,#18322);
#18324=PRESENTATION_STYLE_ASSIGNMENT((#18323));
ENDSEC;
END-ISO-10303-21;
